ISO-10303-21;
HEADER;
FILE_DESCRIPTION (('STEP AP214'),
    '1' );
FILE_NAME ('Actuator Spring Stop Clip.step',
    '2026-10-09T19:32:29',
    ( '' ),
    ( '' ),
    'SwSTEP 2.0',
    'SolidWorks 2026',
    '' );
FILE_SCHEMA (( 'AUTOMOTIVE_DESIGN' ));
ENDSEC;

DATA;
#20=CIRCLE ( 'NONE', #8305, 0.5000000000000000000 ) ;
#29=CARTESIAN_POINT ( 'NONE',  ( 1.850000000000000089, -5.599999999999999645, 6.400000000000000355 ) ) ;
#67=LINE ( 'NONE', #9878, #10862 ) ;
#130=ORIENTED_EDGE ( 'NONE', *, *, #2305, .T. ) ;
#160=CARTESIAN_POINT ( 'NONE',  ( -2.350000000000000089, -5.599999999999999645, 6.400000000000000355 ) ) ;
#163=ORIENTED_EDGE ( 'NONE', *, *, #9591, .T. ) ;
#167=ORIENTED_EDGE ( 'NONE', *, *, #2479, .T. ) ;
#234=CARTESIAN_POINT ( 'NONE',  ( -1.850000000000000089, -6.000000000000000000, 2.799999999999999822 ) ) ;
#261=CARTESIAN_POINT ( 'NONE',  ( -1.850000000000000089, -6.000000000000000000, 6.899999999999999467 ) ) ;
#294=( LENGTH_UNIT ( ) NAMED_UNIT ( * ) SI_UNIT ( .MILLI., .METRE. ) );
#304=CARTESIAN_POINT ( 'NONE',  ( 1.550000000000000044, -5.599999999999999645, 6.100000000000000533 ) ) ;
#354=DIRECTION ( 'NONE',  ( 0.000000000000000000, 0.000000000000000000, 1.000000000000000000 ) ) ;
#380=PRESENTATION_STYLE_ASSIGNMENT (( #14351 ) ) ;
#398=EDGE_CURVE ( 'NONE', #13449, #7267, #12359, .T. ) ;
#399=SHAPE_DEFINITION_REPRESENTATION ( #9174, #16004 ) ;
#412=VERTEX_POINT ( 'NONE', #2819 ) ;
#420=ORIENTED_EDGE ( 'NONE', *, *, #10961, .F. ) ;
#425=PLANE ( 'NONE',  #7325 ) ;
#448=CARTESIAN_POINT ( 'NONE',  ( -1.850000000000000089, -6.000000000000000000, 2.299999999999999822 ) ) ;
#460=SURFACE_SIDE_STYLE ('',( #6019 ) ) ;
#499=ORIENTED_EDGE ( 'NONE', *, *, #14133, .T. ) ;
#520=CARTESIAN_POINT ( 'NONE',  ( 1.550000000000000044, -6.000000000000000000, 5.100000000000000533 ) ) ;
#546=EDGE_LOOP ( 'NONE', ( #14496, #12522, #5384, #16838 ) ) ;
#644=PLANE ( 'NONE',  #2134 ) ;
#698=DIRECTION ( 'NONE',  ( 1.000000000000000000, 0.000000000000000000, 2.865091676452019757E-16 ) ) ;
#715=FACE_OUTER_BOUND ( 'NONE', #5104, .T. ) ;
#917=VERTEX_POINT ( 'NONE', #448 ) ;
#926=AXIS2_PLACEMENT_3D ( 'NONE', #3855, #2475, #9213 ) ;
#934=ADVANCED_FACE ( 'NONE', ( #11744 ), #8962, .T. ) ;
#955=LINE ( 'NONE', #3904, #15604 ) ;
#988=ORIENTED_EDGE ( 'NONE', *, *, #7143, .F. ) ;
#991=CARTESIAN_POINT ( 'NONE',  ( -2.350000000000000089, -5.599999999999999645, 6.400000000000000355 ) ) ;
#1028=EDGE_CURVE ( 'NONE', #13803, #4524, #15525, .T. ) ;
#1036=ORIENTED_EDGE ( 'NONE', *, *, #7213, .F. ) ;
#1046=DIRECTION ( 'NONE',  ( 0.000000000000000000, -1.000000000000000000, 0.000000000000000000 ) ) ;
#1108=VECTOR ( 'NONE', #5713, 1000.000000000000000 ) ;
#1114=EDGE_CURVE ( 'NONE', #7267, #17532, #1440, .T. ) ;
#1125=AXIS2_PLACEMENT_3D ( 'NONE', #14643, #13263, #18230 ) ;
#1205=DIRECTION ( 'NONE',  ( -1.000000000000000000, 0.000000000000000000, 0.000000000000000000 ) ) ;
#1225=CARTESIAN_POINT ( 'NONE',  ( -1.500000000000000000, -5.599999999999999645, 2.299999999999999822 ) ) ;
#1298=VERTEX_POINT ( 'NONE', #1624 ) ;
#1322=ORIENTED_EDGE ( 'NONE', *, *, #14561, .F. ) ;
#1338=ORIENTED_EDGE ( 'NONE', *, *, #7317, .T. ) ;
#1365=ORIENTED_EDGE ( 'NONE', *, *, #5653, .F. ) ;
#1390=FACE_OUTER_BOUND ( 'NONE', #7177, .T. ) ;
#1426=SHAPE_REPRESENTATION_RELATIONSHIP ( 'NONE' , 'NONE' ,  #16004, #6205 ) ;
#1440=LINE ( 'NONE', #11254, #16332 ) ;
#1509=CARTESIAN_POINT ( 'NONE',  ( -1.850000000000000089, -6.000000000000000000, 2.299999999999999822 ) ) ;
#1516=PLANE ( 'NONE',  #10324 ) ;
#1517=VERTEX_POINT ( 'NONE', #160 ) ;
#1518=EDGE_CURVE ( 'NONE', #15430, #7170, #16730, .T. ) ;
#1609=ORIENTED_EDGE ( 'NONE', *, *, #6412, .T. ) ;
#1624=CARTESIAN_POINT ( 'NONE',  ( -1.500000000000000000, -6.000000000000000000, 2.299999999999999822 ) ) ;
#1629=FACE_OUTER_BOUND ( 'NONE', #6040, .T. ) ;
#1687=DIRECTION ( 'NONE',  ( -1.000000000000000000, 0.000000000000000000, 2.220446049250309876E-16 ) ) ;
#1704=AXIS2_PLACEMENT_3D ( 'NONE', #13351, #1798, #7705 ) ;
#1710=VERTEX_POINT ( 'NONE', #7389 ) ;
#1712=VECTOR ( 'NONE', #18175, 1000.000000000000000 ) ;
#1724=ORIENTED_EDGE ( 'NONE', *, *, #5093, .T. ) ;
#1737=CARTESIAN_POINT ( 'NONE',  ( 1.850000000000000089, -5.599999999999999645, 2.299999999999999822 ) ) ;
#1792=VERTEX_POINT ( 'NONE', #13383 ) ;
#1794=PRODUCT_CONTEXT ( 'NONE', #2381, 'mechanical' ) ;
#1798=DIRECTION ( 'NONE',  ( 1.224646799147350002E-16, -1.000000000000000000, -6.123233995736769734E-17 ) ) ;
#1824=ORIENTED_EDGE ( 'NONE', *, *, #10961, .T. ) ;
#1830=DIRECTION ( 'NONE',  ( 0.3420201433256691015, 0.000000000000000000, -0.9396926207859082059 ) ) ;
#1860=LINE ( 'NONE', #3074, #11162 ) ;
#1866=EDGE_LOOP ( 'NONE', ( #12819, #6692, #5571, #10198 ) ) ;
#1868=ORIENTED_EDGE ( 'NONE', *, *, #18146, .T. ) ;
#1935=( NAMED_UNIT ( * ) SI_UNIT ( $, .STERADIAN. ) SOLID_ANGLE_UNIT ( ) );
#1967=PLANE ( 'NONE',  #2632 ) ;
#1973=AXIS2_PLACEMENT_3D ( 'NONE', #234, #8737, #15702 ) ;
#1974=DIRECTION ( 'NONE',  ( -5.551115123125780730E-16, -1.000000000000000000, 0.000000000000000000 ) ) ;
#1975=VECTOR ( 'NONE', #12202, 1000.000000000000000 ) ;
#1983=ADVANCED_FACE ( 'NONE', ( #1390 ), #2788, .T. ) ;
#2029=CARTESIAN_POINT ( 'NONE',  ( -1.850000000000000089, -5.599999999999999645, 2.299999999999999822 ) ) ;
#2044=ORIENTED_EDGE ( 'NONE', *, *, #13220, .T. ) ;
#2116=CARTESIAN_POINT ( 'NONE',  ( -1.000000000000000000, -6.000000000000000000, 5.100000000000000533 ) ) ;
#2121=VERTEX_POINT ( 'NONE', #2116 ) ;
#2134=AXIS2_PLACEMENT_3D ( 'NONE', #6282, #16388, #11942 ) ;
#2145=CARTESIAN_POINT ( 'NONE',  ( 1.850000000000000089, -6.000000000000000000, 6.400000000000000355 ) ) ;
#2194=VERTEX_POINT ( 'NONE', #16656 ) ;
#2301=LINE ( 'NONE', #6552, #12037 ) ;
#2305=EDGE_CURVE ( 'NONE', #1710, #7550, #3894, .T. ) ;
#2341=VERTEX_POINT ( 'NONE', #3700 ) ;
#2381=APPLICATION_CONTEXT ( 'automotive_design' ) ;
#2403=CARTESIAN_POINT ( 'NONE',  ( 1.550000000000000044, -5.599999999999999645, 5.100000000000000533 ) ) ;
#2407=CARTESIAN_POINT ( 'NONE',  ( -1.850000000000000089, -5.599999999999999645, 6.400000000000000355 ) ) ;
#2411=CARTESIAN_POINT ( 'NONE',  ( 1.000000000000000000, -6.000000000000000000, 5.100000000000000533 ) ) ;
#2420=EDGE_LOOP ( 'NONE', ( #15992, #15997, #13998, #17452 ) ) ;
#2475=DIRECTION ( 'NONE',  ( -2.400482215405740060E-16, 0.000000000000000000, 1.000000000000000000 ) ) ;
#2479=EDGE_CURVE ( 'NONE', #14900, #412, #14006, .T. ) ;
#2505=CARTESIAN_POINT ( 'NONE',  ( -1.850000000000000089, -5.599999999999999645, 2.799999999999999822 ) ) ;
#2513=DIRECTION ( 'NONE',  ( -2.220446049250309876E-16, 0.000000000000000000, -1.000000000000000000 ) ) ;
#2630=VERTEX_POINT ( 'NONE', #17641 ) ;
#2632=AXIS2_PLACEMENT_3D ( 'NONE', #7628, #13275, #10482 ) ;
#2633=CARTESIAN_POINT ( 'NONE',  ( -1.000000000000000000, -5.599999999999999645, 5.100000000000000533 ) ) ;
#2685=LINE ( 'NONE', #4155, #13082 ) ;
#2696=CARTESIAN_POINT ( 'NONE',  ( 1.850000000000000089, -5.599999999999999645, 6.400000000000000355 ) ) ;
#2719=EDGE_CURVE ( 'NONE', #14928, #14013, #7995, .T. ) ;
#2731=( NAMED_UNIT ( * ) SI_UNIT ( $, .STERADIAN. ) SOLID_ANGLE_UNIT ( ) );
#2758=DIRECTION ( 'NONE',  ( 0.000000000000000000, -1.000000000000000000, 0.000000000000000000 ) ) ;
#2760=CARTESIAN_POINT ( 'NONE',  ( -2.350000000000000089, -6.000000000000000000, 6.400000000000000355 ) ) ;
#2788=CYLINDRICAL_SURFACE ( 'NONE', #9885, 0.4999999999999995559 ) ;
#2819=CARTESIAN_POINT ( 'NONE',  ( 1.850000000000000089, -5.599999999999999645, 6.899999999999999467 ) ) ;
#2824=CARTESIAN_POINT ( 'NONE',  ( -2.350000000000000089, -5.599999999999999645, 6.400000000000000355 ) ) ;
#2879=DIRECTION ( 'NONE',  ( 0.000000000000000000, 0.000000000000000000, 1.000000000000000000 ) ) ;
#2904=LINE ( 'NONE', #8718, #10631 ) ;
#2918=EDGE_CURVE ( 'NONE', #16759, #1710, #5309, .T. ) ;
#2935=EDGE_CURVE ( 'NONE', #14122, #917, #955, .T. ) ;
#2978=LINE ( 'NONE', #8699, #13290 ) ;
#3013=EDGE_LOOP ( 'NONE', ( #15454, #10603, #8037, #7558 ) ) ;
#3024=FACE_OUTER_BOUND ( 'NONE', #14043, .T. ) ;
#3038=ORIENTED_EDGE ( 'NONE', *, *, #11416, .F. ) ;
#3074=CARTESIAN_POINT ( 'NONE',  ( -1.850000000000000089, -5.599999999999999645, 6.899999999999999467 ) ) ;
#3091=DIRECTION ( 'NONE',  ( 0.000000000000000000, 0.000000000000000000, -1.000000000000000000 ) ) ;
#3098=ORIENTED_EDGE ( 'NONE', *, *, #10545, .F. ) ;
#3113=LINE ( 'NONE', #8674, #14503 ) ;
#3128=DIRECTION ( 'NONE',  ( 0.000000000000000000, -1.000000000000000000, 0.000000000000000000 ) ) ;
#3167=VECTOR ( 'NONE', #8151, 1000.000000000000000 ) ;
#3177=MECHANICAL_DESIGN_GEOMETRIC_PRESENTATION_REPRESENTATION('',(#16775),#15639);
#3204=CARTESIAN_POINT ( 'NONE',  ( -1.850000000000000089, -5.599999999999999645, 2.799999999999999822 ) ) ;
#3217=VECTOR ( 'NONE', #10695, 1000.000000000000000 ) ;
#3247=CARTESIAN_POINT ( 'NONE',  ( 1.000000000000000000, -5.599999999999999645, 5.100000000000000533 ) ) ;
#3256=ADVANCED_FACE ( 'NONE', ( #11495 ), #12713, .T. ) ;
#3350=PLANE ( 'NONE',  #1125 ) ;
#3437=ORIENTED_EDGE ( 'NONE', *, *, #6879, .T. ) ;
#3438=DIRECTION ( 'NONE',  ( -1.556829778943089964E-16, 0.000000000000000000, 1.000000000000000000 ) ) ;
#3471=ORIENTED_EDGE ( 'NONE', *, *, #1518, .F. ) ;
#3510=VECTOR ( 'NONE', #5815, 1000.000000000000000 ) ;
#3566=FACE_OUTER_BOUND ( 'NONE', #7105, .T. ) ;
#3645=DIRECTION ( 'NONE',  ( 0.000000000000000000, 0.000000000000000000, -1.000000000000000000 ) ) ;
#3671=LINE ( 'NONE', #8133, #12395 ) ;
#3700=CARTESIAN_POINT ( 'NONE',  ( -1.550000000000000044, -5.599999999999999645, 6.100000000000000533 ) ) ;
#3748=CARTESIAN_POINT ( 'NONE',  ( 1.850000000000000089, -5.599999999999999645, 2.799999999999999822 ) ) ;
#3768=DIRECTION ( 'NONE',  ( 1.000000000000000000, 0.000000000000000000, -2.220446049250309876E-16 ) ) ;
#3779=CARTESIAN_POINT ( 'NONE',  ( 1.850000000000000089, -5.599999999999999645, 6.899999999999999467 ) ) ;
#3811=ORIENTED_EDGE ( 'NONE', *, *, #1114, .F. ) ;
#3845=DIRECTION ( 'NONE',  ( 1.000000000000000000, 0.000000000000000000, 0.000000000000000000 ) ) ;
#3855=CARTESIAN_POINT ( 'NONE',  ( 1.850000000000000089, -5.599999999999999645, 6.899999999999999467 ) ) ;
#3863=VECTOR ( 'NONE', #6539, 1000.000000000000000 ) ;
#3865=DIRECTION ( 'NONE',  ( 0.000000000000000000, -1.000000000000000000, 0.000000000000000000 ) ) ;
#3878=ORIENTED_EDGE ( 'NONE', *, *, #13264, .T. ) ;
#3894=LINE ( 'NONE', #17669, #15803 ) ;
#3904=CARTESIAN_POINT ( 'NONE',  ( -1.850000000000000089, -5.599999999999999645, 2.299999999999999822 ) ) ;
#3929=ORIENTED_EDGE ( 'NONE', *, *, #9982, .T. ) ;
#3938=LINE ( 'NONE', #13587, #3863 ) ;
#3940=DIRECTION ( 'NONE',  ( 0.000000000000000000, -1.000000000000000000, 0.000000000000000000 ) ) ;
#3941=ADVANCED_FACE ( 'NONE', ( #17834 ), #13614, .T. ) ;
#3981=ORIENTED_EDGE ( 'NONE', *, *, #9111, .T. ) ;
#4000=ORIENTED_EDGE ( 'NONE', *, *, #16070, .F. ) ;
#4028=LINE ( 'NONE', #991, #4914 ) ;
#4072=ORIENTED_EDGE ( 'NONE', *, *, #10168, .T. ) ;
#4106=VERTEX_POINT ( 'NONE', #5579 ) ;
#4112=CARTESIAN_POINT ( 'NONE',  ( -1.550000000000000044, -6.000000000000000000, 6.100000000000000533 ) ) ;
#4129=EDGE_LOOP ( 'NONE', ( #163, #5291, #14228, #16858 ) ) ;
#4137=FACE_OUTER_BOUND ( 'NONE', #10904, .T. ) ;
#4146=DIRECTION ( 'NONE',  ( 1.000000000000000000, 0.000000000000000000, 0.000000000000000000 ) ) ;
#4155=CARTESIAN_POINT ( 'NONE',  ( -1.550000000000000044, -5.599999999999999645, 6.100000000000000533 ) ) ;
#4328=DIRECTION ( 'NONE',  ( 0.3420201433256691015, 0.000000000000000000, 0.9396926207859082059 ) ) ;
#4359=DIRECTION ( 'NONE',  ( -1.000000000000000000, 0.000000000000000000, 0.000000000000000000 ) ) ;
#4371=VERTEX_POINT ( 'NONE', #17478 ) ;
#4397=ORIENTED_EDGE ( 'NONE', *, *, #16070, .T. ) ;
#4413=LINE ( 'NONE', #1737, #12972 ) ;
#4426=EDGE_CURVE ( 'NONE', #7267, #13803, #4999, .T. ) ;
#4458=EDGE_LOOP ( 'NONE', ( #4072, #1609, #13207, #988 ) ) ;
#4497=CARTESIAN_POINT ( 'NONE',  ( 2.350000000000000089, -5.599999999999999645, 2.799999999999999822 ) ) ;
#4524=VERTEX_POINT ( 'NONE', #6370 ) ;
#4556=ORIENTED_EDGE ( 'NONE', *, *, #14675, .F. ) ;
#4561=EDGE_CURVE ( 'NONE', #9915, #14122, #6685, .T. ) ;
#4564=ADVANCED_FACE ( 'NONE', ( #17758 ), #644, .F. ) ;
#4585=VECTOR ( 'NONE', #13058, 1000.000000000000000 ) ;
#4599=EDGE_CURVE ( 'NONE', #2341, #10479, #2685, .T. ) ;
#4654=ORIENTED_EDGE ( 'NONE', *, *, #12073, .T. ) ;
#4680=ORIENTED_EDGE ( 'NONE', *, *, #13128, .T. ) ;
#4738=ORIENTED_EDGE ( 'NONE', *, *, #4426, .T. ) ;
#4804=DIRECTION ( 'NONE',  ( 1.000000000000000000, 0.000000000000000000, 1.556829778943089964E-16 ) ) ;
#4835=LINE ( 'NONE', #9187, #6222 ) ;
#4881=PRODUCT ( 'Actuator Spring Stop Clip', 'Actuator Spring Stop Clip', '', ( #1794 ) ) ;
#4914=VECTOR ( 'NONE', #3940, 1000.000000000000000 ) ;
#4975=EDGE_LOOP ( 'NONE', ( #16712, #12149, #4556, #15480 ) ) ;
#4999=LINE ( 'NONE', #17558, #8759 ) ;
#5066=CARTESIAN_POINT ( 'NONE',  ( -1.500000000000000000, -5.599999999999999645, 2.299999999999999822 ) ) ;
#5093=EDGE_CURVE ( 'NONE', #6773, #2121, #11055, .T. ) ;
#5104=EDGE_LOOP ( 'NONE', ( #4680, #9353, #4000, #3471 ) ) ;
#5201=EDGE_CURVE ( 'NONE', #1517, #9915, #8468, .T. ) ;
#5238=VECTOR ( 'NONE', #9468, 1000.000000000000000 ) ;
#5240=DIRECTION ( 'NONE',  ( 1.224646799147350002E-16, -1.000000000000000000, -6.123233995736769734E-17 ) ) ;
#5291=ORIENTED_EDGE ( 'NONE', *, *, #1518, .T. ) ;
#5297=ORIENTED_EDGE ( 'NONE', *, *, #9111, .F. ) ;
#5309=LINE ( 'NONE', #17778, #5238 ) ;
#5384=ORIENTED_EDGE ( 'NONE', *, *, #12073, .F. ) ;
#5388=ADVANCED_FACE ( 'NONE', ( #10389 ), #3350, .T. ) ;
#5431=EDGE_LOOP ( 'NONE', ( #8535, #1724, #1322, #8680 ) ) ;
#5500=LINE ( 'NONE', #4112, #6790 ) ;
#5571=ORIENTED_EDGE ( 'NONE', *, *, #11390, .F. ) ;
#5579=CARTESIAN_POINT ( 'NONE',  ( -1.850000000000000089, -5.599999999999999645, 6.899999999999999467 ) ) ;
#5588=FACE_OUTER_BOUND ( 'NONE', #8739, .T. ) ;
#5599=( GEOMETRIC_REPRESENTATION_CONTEXT ( 3 ) GLOBAL_UNCERTAINTY_ASSIGNED_CONTEXT ( ( #13805 ) ) GLOBAL_UNIT_ASSIGNED_CONTEXT ( ( #6078, #15511, #2731 ) ) REPRESENTATION_CONTEXT ( 'NONE', 'WORKASPACE' ) );
#5653=EDGE_CURVE ( 'NONE', #4106, #13454, #1860, .T. ) ;
#5663=CARTESIAN_POINT ( 'NONE',  ( -1.850000000000000089, -5.599999999999999645, 6.400000000000000355 ) ) ;
#5713=DIRECTION ( 'NONE',  ( 1.000000000000000000, 0.000000000000000000, 0.000000000000000000 ) ) ;
#5815=DIRECTION ( 'NONE',  ( 0.000000000000000000, -1.000000000000000000, 0.000000000000000000 ) ) ;
#5855=ADVANCED_FACE ( 'NONE', ( #11777 ), #12042, .T. ) ;
#5867=ORIENTED_EDGE ( 'NONE', *, *, #4426, .F. ) ;
#5879=AXIS2_PLACEMENT_3D ( 'NONE', #2407, #16459, #13696 ) ;
#5965=CARTESIAN_POINT ( 'NONE',  ( -1.000000000000000000, -5.599999999999999645, 3.673738709727309981 ) ) ;
#5982=ORIENTED_EDGE ( 'NONE', *, *, #1114, .T. ) ;
#6019=SURFACE_STYLE_FILL_AREA ( #8708 ) ;
#6021=AXIS2_PLACEMENT_3D ( 'NONE', #2696, #11303, #14178 ) ;
#6040=EDGE_LOOP ( 'NONE', ( #12850, #3981, #13950, #18004, #6655, #4397, #3929, #130, #9619, #7782, #13883, #16137, #1338, #4654, #1868, #13602, #3878, #10188 ) ) ;
#6078=( LENGTH_UNIT ( ) NAMED_UNIT ( * ) SI_UNIT ( .MILLI., .METRE. ) );
#6190=PRODUCT_DEFINITION_FORMATION_WITH_SPECIFIED_SOURCE ( 'ANY', '', #4881, .NOT_KNOWN. ) ;
#6198=DIRECTION ( 'NONE',  ( 0.000000000000000000, 1.000000000000000000, 0.000000000000000000 ) ) ;
#6205=ADVANCED_BREP_SHAPE_REPRESENTATION ( '', ( #7785, #17681 ), #5599 ) ;
#6222=VECTOR ( 'NONE', #3438, 1000.000000000000000 ) ;
#6261=CARTESIAN_POINT ( 'NONE',  ( -1.000000000000000000, -6.000000000000000000, 3.673738709727309981 ) ) ;
#6282=CARTESIAN_POINT ( 'NONE',  ( 0.000000000000000000, -5.599999999999999645, -3.429011037612589769E-16 ) ) ;
#6349=CARTESIAN_POINT ( 'NONE',  ( -1.550000000000000044, -5.599999999999999645, 5.100000000000000533 ) ) ;
#6370=CARTESIAN_POINT ( 'NONE',  ( 1.850000000000000089, -5.599999999999999645, 2.299999999999999822 ) ) ;
#6381=ORIENTED_EDGE ( 'NONE', *, *, #2479, .F. ) ;
#6412=EDGE_CURVE ( 'NONE', #1792, #14614, #9064, .T. ) ;
#6414=LINE ( 'NONE', #17598, #10239 ) ;
#6539=DIRECTION ( 'NONE',  ( -1.000000000000000000, 0.000000000000000000, -2.400482215405740060E-16 ) ) ;
#6552=CARTESIAN_POINT ( 'NONE',  ( -1.550000000000000044, -6.000000000000000000, 5.100000000000000533 ) ) ;
#6562=ORIENTED_EDGE ( 'NONE', *, *, #13220, .F. ) ;
#6598=ORIENTED_EDGE ( 'NONE', *, *, #12778, .F. ) ;
#6599=ORIENTED_EDGE ( 'NONE', *, *, #9271, .F. ) ;
#6632=CARTESIAN_POINT ( 'NONE',  ( -2.350000000000000089, -5.599999999999999645, 2.799999999999999822 ) ) ;
#6655=ORIENTED_EDGE ( 'NONE', *, *, #8689, .T. ) ;
#6685=CIRCLE ( 'NONE', #16744, 0.5000000000000000000 ) ;
#6690=ORIENTED_EDGE ( 'NONE', *, *, #16927, .F. ) ;
#6692=ORIENTED_EDGE ( 'NONE', *, *, #7219, .T. ) ;
#6773=VERTEX_POINT ( 'NONE', #8123 ) ;
#6790=VECTOR ( 'NONE', #16624, 1000.000000000000000 ) ;
#6834=VERTEX_POINT ( 'NONE', #16355 ) ;
#6853=CARTESIAN_POINT ( 'NONE',  ( 2.350000000000000089, -6.000000000000000000, 6.400000000000000355 ) ) ;
#6879=EDGE_CURVE ( 'NONE', #1517, #4371, #4028, .T. ) ;
#6949=UNCERTAINTY_MEASURE_WITH_UNIT (LENGTH_MEASURE( 1.000000000000000082E-05 ), #294, 'distance_accuracy_value', 'NONE');
#6955=PLANE ( 'NONE',  #14115 ) ;
#7105=EDGE_LOOP ( 'NONE', ( #15868, #14343, #6598, #420 ) ) ;
#7115=LINE ( 'NONE', #2760, #1712 ) ;
#7142=CARTESIAN_POINT ( 'NONE',  ( 1.550000000000000044, -5.599999999999999645, 5.100000000000000533 ) ) ;
#7143=EDGE_CURVE ( 'NONE', #15958, #1298, #67, .T. ) ;
#7170=VERTEX_POINT ( 'NONE', #8750 ) ;
#7177=EDGE_LOOP ( 'NONE', ( #2044, #3437, #15737, #1365 ) ) ;
#7188=EDGE_LOOP ( 'NONE', ( #13030, #6562, #12055, #6381, #3038, #12153, #8984, #5867, #11753, #12573, #3098, #18277, #12033, #9281, #13708, #14050, #1036, #16446 ) ) ;
#7192=DIRECTION ( 'NONE',  ( 0.000000000000000000, 0.000000000000000000, -1.000000000000000000 ) ) ;
#7213=EDGE_CURVE ( 'NONE', #14122, #15958, #11532, .T. ) ;
#7219=EDGE_CURVE ( 'NONE', #13449, #11068, #14037, .T. ) ;
#7267=VERTEX_POINT ( 'NONE', #8289 ) ;
#7279=CARTESIAN_POINT ( 'NONE',  ( 1.000000000000000000, -5.599999999999999645, 5.100000000000000533 ) ) ;
#7317=EDGE_CURVE ( 'NONE', #6834, #14013, #11464, .T. ) ;
#7325=AXIS2_PLACEMENT_3D ( 'NONE', #14500, #10408, #14316 ) ;
#7377=DIRECTION ( 'NONE',  ( 0.000000000000000000, -1.000000000000000000, 0.000000000000000000 ) ) ;
#7389=CARTESIAN_POINT ( 'NONE',  ( 1.550000000000000044, -6.000000000000000000, 6.100000000000000533 ) ) ;
#7479=ORIENTED_EDGE ( 'NONE', *, *, #2935, .T. ) ;
#7543=FACE_OUTER_BOUND ( 'NONE', #4975, .T. ) ;
#7550=VERTEX_POINT ( 'NONE', #11032 ) ;
#7554=CARTESIAN_POINT ( 'NONE',  ( 1.000000000000000000, -6.000000000000000000, 5.100000000000000533 ) ) ;
#7558=ORIENTED_EDGE ( 'NONE', *, *, #13367, .F. ) ;
#7597=ORIENTED_EDGE ( 'NONE', *, *, #18146, .F. ) ;
#7628=CARTESIAN_POINT ( 'NONE',  ( 4.898587196589409994E-17, -6.000000000000000000, -3.673940397442060361E-16 ) ) ;
#7629=VECTOR ( 'NONE', #14722, 1000.000000000000000 ) ;
#7653=CARTESIAN_POINT ( 'NONE',  ( 2.350000000000000089, -6.000000000000000000, 2.799999999999999822 ) ) ;
#7690=CARTESIAN_POINT ( 'NONE',  ( -1.000000000000000000, -5.599999999999999645, 3.673738709727309981 ) ) ;
#7705=DIRECTION ( 'NONE',  ( 0.000000000000000000, 0.000000000000000000, -1.000000000000000000 ) ) ;
#7708=ORIENTED_EDGE ( 'NONE', *, *, #15065, .T. ) ;
#7782=ORIENTED_EDGE ( 'NONE', *, *, #11308, .T. ) ;
#7785=MANIFOLD_SOLID_BREP ( 'Stock-MAS-687-1', #17327 ) ;
#7798=APPLICATION_CONTEXT ( 'automotive_design' ) ;
#7925=CARTESIAN_POINT ( 'NONE',  ( -1.850000000000000089, -5.599999999999999645, 2.299999999999999822 ) ) ;
#7995=LINE ( 'NONE', #12430, #8543 ) ;
#8037=ORIENTED_EDGE ( 'NONE', *, *, #7317, .F. ) ;
#8050=LINE ( 'NONE', #17738, #11149 ) ;
#8123=CARTESIAN_POINT ( 'NONE',  ( -1.000000000000000000, -5.599999999999999645, 5.100000000000000533 ) ) ;
#8133=CARTESIAN_POINT ( 'NONE',  ( 1.500000000000000000, -6.000000000000000000, 2.299999999999999822 ) ) ;
#8151=DIRECTION ( 'NONE',  ( 0.000000000000000000, -1.000000000000000000, 0.000000000000000000 ) ) ;
#8250=AXIS2_PLACEMENT_3D ( 'NONE', #9795, #11274, #8495 ) ;
#8289=CARTESIAN_POINT ( 'NONE',  ( 1.000000000000000000, -5.599999999999999645, 3.673738709727309981 ) ) ;
#8305=AXIS2_PLACEMENT_3D ( 'NONE', #3748, #5240, #12100 ) ;
#8309=FACE_OUTER_BOUND ( 'NONE', #9892, .T. ) ;
#8317=AXIS2_PLACEMENT_3D ( 'NONE', #11263, #7192, #11070 ) ;
#8325=DIRECTION ( 'NONE',  ( 0.000000000000000000, -1.000000000000000000, 0.000000000000000000 ) ) ;
#8351=ADVANCED_FACE ( 'NONE', ( #1629 ), #1967, .T. ) ;
#8375=PLANE ( 'NONE',  #12682 ) ;
#8388=CARTESIAN_POINT ( 'NONE',  ( 1.500000000000000000, -5.599999999999999645, 2.299999999999999822 ) ) ;
#8421=DIRECTION ( 'NONE',  ( 0.000000000000000000, -1.000000000000000000, 0.000000000000000000 ) ) ;
#8451=ORIENTED_EDGE ( 'NONE', *, *, #2935, .F. ) ;
#8468=LINE ( 'NONE', #2824, #17651 ) ;
#8495=DIRECTION ( 'NONE',  ( -0.3420201433256691015, 0.000000000000000000, 0.9396926207859082059 ) ) ;
#8535=ORIENTED_EDGE ( 'NONE', *, *, #11874, .T. ) ;
#8543=VECTOR ( 'NONE', #10855, 1000.000000000000000 ) ;
#8545=LINE ( 'NONE', #1509, #15358 ) ;
#8549=DIRECTION ( 'NONE',  ( 0.000000000000000000, -1.000000000000000000, 0.000000000000000000 ) ) ;
#8550=DIRECTION ( 'NONE',  ( 0.000000000000000000, 1.000000000000000000, 0.000000000000000000 ) ) ;
#8565=CARTESIAN_POINT ( 'NONE',  ( -1.550000000000000044, -5.599999999999999645, 5.100000000000000533 ) ) ;
#8591=DIRECTION ( 'NONE',  ( 0.000000000000000000, -1.000000000000000000, 0.000000000000000000 ) ) ;
#8632=DIRECTION ( 'NONE',  ( 0.000000000000000000, 0.000000000000000000, 1.000000000000000000 ) ) ;
#8674=CARTESIAN_POINT ( 'NONE',  ( 1.000000000000000000, -6.000000000000000000, 3.673738709727309981 ) ) ;
#8680=ORIENTED_EDGE ( 'NONE', *, *, #6412, .F. ) ;
#8689=EDGE_CURVE ( 'NONE', #2121, #7170, #14905, .T. ) ;
#8699=CARTESIAN_POINT ( 'NONE',  ( 1.550000000000000044, -5.599999999999999645, 6.100000000000000533 ) ) ;
#8708=FILL_AREA_STYLE ('',( #10447 ) ) ;
#8718=CARTESIAN_POINT ( 'NONE',  ( -1.500000000000000000, -5.599999999999999645, 2.299999999999999822 ) ) ;
#8737=DIRECTION ( 'NONE',  ( 1.224646799147350002E-16, -1.000000000000000000, -6.123233995736769734E-17 ) ) ;
#8739=EDGE_LOOP ( 'NONE', ( #11161, #499, #17769, #9552 ) ) ;
#8750=CARTESIAN_POINT ( 'NONE',  ( -1.550000000000000044, -6.000000000000000000, 5.100000000000000533 ) ) ;
#8759=VECTOR ( 'NONE', #15111, 1000.000000000000227 ) ;
#8872=VECTOR ( 'NONE', #17831, 1000.000000000000000 ) ;
#8938=VERTEX_POINT ( 'NONE', #11692 ) ;
#8950=LINE ( 'NONE', #7653, #9479 ) ;
#8956=VECTOR ( 'NONE', #8325, 1000.000000000000000 ) ;
#8962=PLANE ( 'NONE',  #16051 ) ;
#8984=ORIENTED_EDGE ( 'NONE', *, *, #1028, .F. ) ;
#9007=ADVANCED_FACE ( 'NONE', ( #11575 ), #11403, .T. ) ;
#9064=LINE ( 'NONE', #5965, #7629 ) ;
#9111=EDGE_CURVE ( 'NONE', #917, #1298, #8545, .T. ) ;
#9162=VECTOR ( 'NONE', #17449, 1000.000000000000000 ) ;
#9174=PRODUCT_DEFINITION_SHAPE ( 'NONE', 'NONE',  #12313 ) ;
#9187=CARTESIAN_POINT ( 'NONE',  ( -1.000000000000000000, -5.599999999999999645, 3.673738709727309981 ) ) ;
#9213=DIRECTION ( 'NONE',  ( 1.000000000000000000, 0.000000000000000000, 2.400482215405740060E-16 ) ) ;
#9223=LINE ( 'NONE', #6261, #1975 ) ;
#9271=EDGE_CURVE ( 'NONE', #8938, #6834, #3671, .T. ) ;
#9281=ORIENTED_EDGE ( 'NONE', *, *, #9591, .F. ) ;
#9353=ORIENTED_EDGE ( 'NONE', *, *, #4599, .T. ) ;
#9450=DIRECTION ( 'NONE',  ( -1.000000000000000000, 0.000000000000000000, 0.000000000000000000 ) ) ;
#9468=DIRECTION ( 'NONE',  ( 0.000000000000000000, -1.000000000000000000, 0.000000000000000000 ) ) ;
#9479=VECTOR ( 'NONE', #354, 1000.000000000000000 ) ;
#9499=VECTOR ( 'NONE', #10464, 1000.000000000000000 ) ;
#9538=CARTESIAN_POINT ( 'NONE',  ( 1.550000000000000044, -5.599999999999999645, 5.100000000000000533 ) ) ;
#9549=VECTOR ( 'NONE', #3845, 1000.000000000000000 ) ;
#9552=ORIENTED_EDGE ( 'NONE', *, *, #2918, .F. ) ;
#9591=EDGE_CURVE ( 'NONE', #6773, #15430, #16430, .T. ) ;
#9605=ORIENTED_EDGE ( 'NONE', *, *, #11308, .F. ) ;
#9619=ORIENTED_EDGE ( 'NONE', *, *, #11390, .T. ) ;
#9631=ADVANCED_FACE ( 'NONE', ( #11594 ), #17223, .T. ) ;
#9649=ORIENTED_EDGE ( 'NONE', *, *, #1028, .T. ) ;
#9676=COLOUR_RGB ( '', 0.72549020, 0.75294118, 0.79215686) ;
#9699=CARTESIAN_POINT ( 'NONE',  ( -1.850000000000000089, -6.000000000000000000, 6.400000000000000355 ) ) ;
#9739=AXIS2_PLACEMENT_3D ( 'NONE', #15862, #13081, #6198 ) ;
#9762=EDGE_CURVE ( 'NONE', #14900, #15707, #10241, .T. ) ;
#9787=CARTESIAN_POINT ( 'NONE',  ( -1.850000000000000089, -5.599999999999999645, 2.299999999999999822 ) ) ;
#9795=CARTESIAN_POINT ( 'NONE',  ( 1.000000000000000000, -5.599999999999999645, 3.673738709727309981 ) ) ;
#9878=CARTESIAN_POINT ( 'NONE',  ( -1.500000000000000000, -5.599999999999999645, 2.299999999999999822 ) ) ;
#9885=AXIS2_PLACEMENT_3D ( 'NONE', #5663, #9912, #2879 ) ;
#9892=EDGE_LOOP ( 'NONE', ( #9649, #12767, #6599, #15670 ) ) ;
#9912=DIRECTION ( 'NONE',  ( 1.224646799147350002E-16, -1.000000000000000000, -6.123233995736759873E-17 ) ) ;
#9915=VERTEX_POINT ( 'NONE', #6632 ) ;
#9972=CARTESIAN_POINT ( 'NONE',  ( 2.350000000000000089, -5.599999999999999645, 6.400000000000000355 ) ) ;
#9982=EDGE_CURVE ( 'NONE', #10479, #1710, #5500, .T. ) ;
#9986=CIRCLE ( 'NONE', #1973, 0.5000000000000000000 ) ;
#10063=ADVANCED_FACE ( 'NONE', ( #5588 ), #1516, .T. ) ;
#10168=EDGE_CURVE ( 'NONE', #15958, #1792, #2904, .T. ) ;
#10182=DIRECTION ( 'NONE',  ( 1.000000000000000000, 0.000000000000000000, 0.000000000000000000 ) ) ;
#10188=ORIENTED_EDGE ( 'NONE', *, *, #14675, .T. ) ;
#10198=ORIENTED_EDGE ( 'NONE', *, *, #14133, .F. ) ;
#10239=VECTOR ( 'NONE', #1974, 1000.000000000000000 ) ;
#10241=LINE ( 'NONE', #12856, #3510 ) ;
#10256=VECTOR ( 'NONE', #4328, 1000.000000000000227 ) ;
#10273=( NAMED_UNIT ( * ) PLANE_ANGLE_UNIT ( ) SI_UNIT ( $, .RADIAN. ) );
#10294=DIRECTION ( 'NONE',  ( 1.000000000000000000, 0.000000000000000000, 0.000000000000000000 ) ) ;
#10297=CIRCLE ( 'NONE', #5879, 0.4999999999999995559 ) ;
#10324=AXIS2_PLACEMENT_3D ( 'NONE', #304, #1687, #8550 ) ;
#10337=DIRECTION ( 'NONE',  ( 0.000000000000000000, 0.000000000000000000, -1.000000000000000000 ) ) ;
#10389=FACE_OUTER_BOUND ( 'NONE', #1866, .T. ) ;
#10408=DIRECTION ( 'NONE',  ( -1.000000000000000000, 0.000000000000000000, 0.000000000000000000 ) ) ;
#10447=FILL_AREA_STYLE_COLOUR ( '', #9676 ) ;
#10464=DIRECTION ( 'NONE',  ( -1.000000000000000000, 0.000000000000000000, -2.400482215405740060E-16 ) ) ;
#10479=VERTEX_POINT ( 'NONE', #10658 ) ;
#10482=DIRECTION ( 'NONE',  ( 0.000000000000000000, 6.123233995736769734E-17, -1.000000000000000000 ) ) ;
#10545=EDGE_CURVE ( 'NONE', #16759, #16005, #2978, .T. ) ;
#10603=ORIENTED_EDGE ( 'NONE', *, *, #2719, .T. ) ;
#10627=PLANE ( 'NONE',  #17049 ) ;
#10631=VECTOR ( 'NONE', #12891, 1000.000000000000227 ) ;
#10658=CARTESIAN_POINT ( 'NONE',  ( -1.550000000000000044, -6.000000000000000000, 6.100000000000000533 ) ) ;
#10695=DIRECTION ( 'NONE',  ( -1.000000000000000000, 0.000000000000000000, 0.000000000000000000 ) ) ;
#10794=LINE ( 'NONE', #17615, #11539 ) ;
#10855=DIRECTION ( 'NONE',  ( 0.000000000000000000, -1.000000000000000000, 0.000000000000000000 ) ) ;
#10862=VECTOR ( 'NONE', #2758, 1000.000000000000000 ) ;
#10882=CARTESIAN_POINT ( 'NONE',  ( -1.000000000000000000, -5.599999999999999645, 5.100000000000000533 ) ) ;
#10904=EDGE_LOOP ( 'NONE', ( #4738, #7708, #11795, #3811 ) ) ;
#10917=CARTESIAN_POINT ( 'NONE',  ( -1.550000000000000044, -5.599999999999999645, 5.100000000000000533 ) ) ;
#10961=EDGE_CURVE ( 'NONE', #412, #2630, #15185, .T. ) ;
#11000=DIRECTION ( 'NONE',  ( 1.000000000000000000, 0.000000000000000000, 0.000000000000000000 ) ) ;
#11032=CARTESIAN_POINT ( 'NONE',  ( 1.550000000000000044, -6.000000000000000000, 5.100000000000000533 ) ) ;
#11055=LINE ( 'NONE', #12364, #14139 ) ;
#11068=VERTEX_POINT ( 'NONE', #2411 ) ;
#11070=DIRECTION ( 'NONE',  ( 0.000000000000000000, -1.000000000000000000, 0.000000000000000000 ) ) ;
#11107=DIRECTION ( 'NONE',  ( -2.220446049250309876E-16, 0.000000000000000000, -1.000000000000000000 ) ) ;
#11149=VECTOR ( 'NONE', #3865, 1000.000000000000000 ) ;
#11161=ORIENTED_EDGE ( 'NONE', *, *, #10545, .T. ) ;
#11162=VECTOR ( 'NONE', #8549, 1000.000000000000000 ) ;
#11191=CARTESIAN_POINT ( 'NONE',  ( 0.000000000000000000, 0.000000000000000000, 0.000000000000000000 ) ) ;
#11252=CARTESIAN_POINT ( 'NONE',  ( 1.550000000000000044, -5.599999999999999645, 6.100000000000000533 ) ) ;
#11254=CARTESIAN_POINT ( 'NONE',  ( 1.000000000000000000, -5.599999999999999645, 3.673738709727309981 ) ) ;
#11263=CARTESIAN_POINT ( 'NONE',  ( 1.500000000000000000, -5.599999999999999645, 2.299999999999999822 ) ) ;
#11274=DIRECTION ( 'NONE',  ( -0.9396926207859082059, 3.797186380057531567E-16, -0.3420201433256691015 ) ) ;
#11303=DIRECTION ( 'NONE',  ( 1.224646799147350002E-16, -1.000000000000000000, -6.123233995736769734E-17 ) ) ;
#11308=EDGE_CURVE ( 'NONE', #11068, #17532, #16920, .T. ) ;
#11365=PLANE ( 'NONE',  #8250 ) ;
#11390=EDGE_CURVE ( 'NONE', #7550, #11068, #11544, .T. ) ;
#11403=PLANE ( 'NONE',  #14455 ) ;
#11416=EDGE_CURVE ( 'NONE', #14928, #14900, #13293, .T. ) ;
#11451=EDGE_CURVE ( 'NONE', #17532, #8938, #3113, .T. ) ;
#11464=CIRCLE ( 'NONE', #1704, 0.5000000000000000000 ) ;
#11495=FACE_OUTER_BOUND ( 'NONE', #13346, .T. ) ;
#11532=LINE ( 'NONE', #9787, #1108 ) ;
#11539=VECTOR ( 'NONE', #698, 1000.000000000000000 ) ;
#11544=LINE ( 'NONE', #520, #9162 ) ;
#11553=EDGE_CURVE ( 'NONE', #2341, #16759, #10794, .T. ) ;
#11572=EDGE_CURVE ( 'NONE', #4524, #14928, #20, .T. ) ;
#11575=FACE_OUTER_BOUND ( 'NONE', #13507, .T. ) ;
#11594=FACE_OUTER_BOUND ( 'NONE', #546, .T. ) ;
#11625=CARTESIAN_POINT ( 'NONE',  ( 1.000000000000000000, -5.599999999999999645, 5.100000000000000533 ) ) ;
#11692=CARTESIAN_POINT ( 'NONE',  ( 1.500000000000000000, -6.000000000000000000, 2.299999999999999822 ) ) ;
#11744=FACE_OUTER_BOUND ( 'NONE', #16834, .T. ) ;
#11751=AXIS2_PLACEMENT_3D ( 'NONE', #12403, #15000, #15190 ) ;
#11753=ORIENTED_EDGE ( 'NONE', *, *, #398, .F. ) ;
#11777=FACE_OUTER_BOUND ( 'NONE', #5431, .T. ) ;
#11795=ORIENTED_EDGE ( 'NONE', *, *, #11451, .F. ) ;
#11815=CYLINDRICAL_SURFACE ( 'NONE', #13534, 0.5000000000000000000 ) ;
#11874=EDGE_CURVE ( 'NONE', #1792, #6773, #4835, .T. ) ;
#11876=CARTESIAN_POINT ( 'NONE',  ( 1.850000000000000089, -6.000000000000000000, 6.899999999999999467 ) ) ;
#11942=DIRECTION ( 'NONE',  ( 0.000000000000000000, 6.123233995736769734E-17, -1.000000000000000000 ) ) ;
#12013=DIRECTION ( 'NONE',  ( -2.220446049250309876E-16, 0.000000000000000000, -1.000000000000000000 ) ) ;
#12030=DIRECTION ( 'NONE',  ( -1.000000000000000000, 0.000000000000000000, 0.000000000000000000 ) ) ;
#12033=ORIENTED_EDGE ( 'NONE', *, *, #13128, .F. ) ;
#12037=VECTOR ( 'NONE', #14988, 1000.000000000000000 ) ;
#12042=PLANE ( 'NONE',  #12947 ) ;
#12055=ORIENTED_EDGE ( 'NONE', *, *, #12439, .F. ) ;
#12066=ORIENTED_EDGE ( 'NONE', *, *, #398, .T. ) ;
#12073=EDGE_CURVE ( 'NONE', #14013, #15707, #8950, .T. ) ;
#12100=DIRECTION ( 'NONE',  ( 0.000000000000000000, 0.000000000000000000, -1.000000000000000000 ) ) ;
#12123=DIRECTION ( 'NONE',  ( 2.220446049250309876E-16, 0.000000000000000000, 1.000000000000000000 ) ) ;
#12149=ORIENTED_EDGE ( 'NONE', *, *, #16050, .T. ) ;
#12153=ORIENTED_EDGE ( 'NONE', *, *, #11572, .F. ) ;
#12202=DIRECTION ( 'NONE',  ( -1.556829778943089964E-16, 0.000000000000000000, 1.000000000000000000 ) ) ;
#12284=CARTESIAN_POINT ( 'NONE',  ( 1.000000000000000000, -6.000000000000000000, 3.673738709727309981 ) ) ;
#12313=PRODUCT_DEFINITION ( 'UNKNOWN', '', #6190, #16593 ) ;
#12315=ADVANCED_FACE ( 'NONE', ( #3566 ), #14877, .T. ) ;
#12359=LINE ( 'NONE', #16972, #4585 ) ;
#12364=CARTESIAN_POINT ( 'NONE',  ( -1.000000000000000000, -5.599999999999999645, 5.100000000000000533 ) ) ;
#12380=CYLINDRICAL_SURFACE ( 'NONE', #14724, 0.5000000000000000000 ) ;
#12395=VECTOR ( 'NONE', #11000, 1000.000000000000000 ) ;
#12403=CARTESIAN_POINT ( 'NONE',  ( -1.550000000000000044, -5.599999999999999645, 6.100000000000000533 ) ) ;
#12430=CARTESIAN_POINT ( 'NONE',  ( 2.350000000000000089, -5.599999999999999645, 2.799999999999999822 ) ) ;
#12439=EDGE_CURVE ( 'NONE', #412, #4106, #3938, .T. ) ;
#12479=ADVANCED_FACE ( 'NONE', ( #8309 ), #15533, .T. ) ;
#12499=LINE ( 'NONE', #7142, #16173 ) ;
#12522=ORIENTED_EDGE ( 'NONE', *, *, #9762, .T. ) ;
#12573=ORIENTED_EDGE ( 'NONE', *, *, #15769, .F. ) ;
#12627=VECTOR ( 'NONE', #7377, 1000.000000000000000 ) ;
#12677=AXIS2_PLACEMENT_3D ( 'NONE', #9699, #14145, #15545 ) ;
#12682=AXIS2_PLACEMENT_3D ( 'NONE', #2633, #15227, #16694 ) ;
#12713=CYLINDRICAL_SURFACE ( 'NONE', #17377, 0.5000000000000000000 ) ;
#12739=DIRECTION ( 'NONE',  ( 0.000000000000000000, -1.000000000000000000, -1.110223024625160090E-15 ) ) ;
#12767=ORIENTED_EDGE ( 'NONE', *, *, #13367, .T. ) ;
#12775=CARTESIAN_POINT ( 'NONE',  ( -1.500000000000000000, -6.000000000000000000, 2.299999999999999822 ) ) ;
#12778=EDGE_CURVE ( 'NONE', #2630, #13454, #16313, .T. ) ;
#12819=ORIENTED_EDGE ( 'NONE', *, *, #15769, .T. ) ;
#12850=ORIENTED_EDGE ( 'NONE', *, *, #16927, .T. ) ;
#12856=CARTESIAN_POINT ( 'NONE',  ( 2.350000000000000089, -5.599999999999999645, 6.400000000000000355 ) ) ;
#12883=DIRECTION ( 'NONE',  ( 1.224646799147350002E-16, -1.000000000000000000, -6.123233995736759873E-17 ) ) ;
#12891=DIRECTION ( 'NONE',  ( 0.3420201433256691015, 0.000000000000000000, 0.9396926207859082059 ) ) ;
#12947=AXIS2_PLACEMENT_3D ( 'NONE', #7690, #4804, #17665 ) ;
#12972=VECTOR ( 'NONE', #8591, 1000.000000000000000 ) ;
#13030=ORIENTED_EDGE ( 'NONE', *, *, #5201, .F. ) ;
#13052=ORIENTED_EDGE ( 'NONE', *, *, #16050, .F. ) ;
#13058=DIRECTION ( 'NONE',  ( 0.000000000000000000, 0.000000000000000000, -1.000000000000000000 ) ) ;
#13081=DIRECTION ( 'NONE',  ( 1.000000000000000000, 0.000000000000000000, 0.000000000000000000 ) ) ;
#13082=VECTOR ( 'NONE', #8421, 1000.000000000000000 ) ;
#13114=DIRECTION ( 'NONE',  ( -1.000000000000000000, 0.000000000000000000, 0.000000000000000000 ) ) ;
#13128=EDGE_CURVE ( 'NONE', #15430, #2341, #17547, .T. ) ;
#13207=ORIENTED_EDGE ( 'NONE', *, *, #14173, .F. ) ;
#13220=EDGE_CURVE ( 'NONE', #4106, #1517, #10297, .T. ) ;
#13231=CARTESIAN_POINT ( 'NONE',  ( -1.000000000000000000, -6.000000000000000000, 5.100000000000000533 ) ) ;
#13263=DIRECTION ( 'NONE',  ( 0.000000000000000000, 0.000000000000000000, 1.000000000000000000 ) ) ;
#13264=EDGE_CURVE ( 'NONE', #13454, #4371, #17973, .T. ) ;
#13275=DIRECTION ( 'NONE',  ( 1.224646799147350002E-16, -1.000000000000000000, -6.123233995736769734E-17 ) ) ;
#13290=VECTOR ( 'NONE', #11107, 1000.000000000000000 ) ;
#13293=LINE ( 'NONE', #4497, #15696 ) ;
#13324=ADVANCED_FACE ( 'NONE', ( #4137 ), #11365, .T. ) ;
#13330=DIRECTION ( 'NONE',  ( 1.224646799147350002E-16, -1.000000000000000000, -6.123233995736769734E-17 ) ) ;
#13346=EDGE_LOOP ( 'NONE', ( #167, #1824, #7597, #17622 ) ) ;
#13351=CARTESIAN_POINT ( 'NONE',  ( 1.850000000000000089, -6.000000000000000000, 2.799999999999999822 ) ) ;
#13367=EDGE_CURVE ( 'NONE', #4524, #6834, #4413, .T. ) ;
#13383=CARTESIAN_POINT ( 'NONE',  ( -1.000000000000000000, -5.599999999999999645, 3.673738709727309981 ) ) ;
#13439=DIRECTION ( 'NONE',  ( 1.224646799147350002E-16, -1.000000000000000000, -6.123233995736769734E-17 ) ) ;
#13449=VERTEX_POINT ( 'NONE', #11625 ) ;
#13454=VERTEX_POINT ( 'NONE', #261 ) ;
#13507=EDGE_LOOP ( 'NONE', ( #12066, #5982, #9605, #13702 ) ) ;
#13534=AXIS2_PLACEMENT_3D ( 'NONE', #3204, #14405, #13114 ) ;
#13553=VECTOR ( 'NONE', #12123, 1000.000000000000000 ) ;
#13587=CARTESIAN_POINT ( 'NONE',  ( 1.850000000000000089, -5.599999999999999645, 6.899999999999999467 ) ) ;
#13602=ORIENTED_EDGE ( 'NONE', *, *, #12778, .T. ) ;
#13614=PLANE ( 'NONE',  #11751 ) ;
#13696=DIRECTION ( 'NONE',  ( 0.000000000000000000, 0.000000000000000000, 1.000000000000000000 ) ) ;
#13702=ORIENTED_EDGE ( 'NONE', *, *, #7219, .F. ) ;
#13708=ORIENTED_EDGE ( 'NONE', *, *, #11874, .F. ) ;
#13803=VERTEX_POINT ( 'NONE', #15706 ) ;
#13805=UNCERTAINTY_MEASURE_WITH_UNIT (LENGTH_MEASURE( 1.000000000000000082E-05 ), #6078, 'distance_accuracy_value', 'NONE');
#13883=ORIENTED_EDGE ( 'NONE', *, *, #11451, .T. ) ;
#13911=FACE_OUTER_BOUND ( 'NONE', #4458, .T. ) ;
#13924=ADVANCED_FACE ( 'NONE', ( #13911 ), #6955, .T. ) ;
#13950=ORIENTED_EDGE ( 'NONE', *, *, #14173, .T. ) ;
#13998=ORIENTED_EDGE ( 'NONE', *, *, #9982, .F. ) ;
#14006=CIRCLE ( 'NONE', #6021, 0.5000000000000000000 ) ;
#14013=VERTEX_POINT ( 'NONE', #17289 ) ;
#14037=LINE ( 'NONE', #7279, #12627 ) ;
#14043=EDGE_LOOP ( 'NONE', ( #16422, #7479, #6690, #13052 ) ) ;
#14050=ORIENTED_EDGE ( 'NONE', *, *, #10168, .F. ) ;
#14115=AXIS2_PLACEMENT_3D ( 'NONE', #1225, #18129, #15678 ) ;
#14122=VERTEX_POINT ( 'NONE', #2029 ) ;
#14133=EDGE_CURVE ( 'NONE', #16005, #7550, #16475, .T. ) ;
#14139=VECTOR ( 'NONE', #17985, 1000.000000000000000 ) ;
#14145=DIRECTION ( 'NONE',  ( 1.224646799147350002E-16, -1.000000000000000000, -6.123233995736769734E-17 ) ) ;
#14173=EDGE_CURVE ( 'NONE', #1298, #14614, #17012, .T. ) ;
#14178=DIRECTION ( 'NONE',  ( 1.000000000000000000, 0.000000000000000000, 0.000000000000000000 ) ) ;
#14184=ORIENTED_EDGE ( 'NONE', *, *, #7143, .T. ) ;
#14228=ORIENTED_EDGE ( 'NONE', *, *, #8689, .F. ) ;
#14314=CARTESIAN_POINT ( 'NONE',  ( 2.350000000000000089, -5.599999999999999645, 2.799999999999999822 ) ) ;
#14316=DIRECTION ( 'NONE',  ( 0.000000000000000000, 0.000000000000000000, 1.000000000000000000 ) ) ;
#14343=ORIENTED_EDGE ( 'NONE', *, *, #5653, .T. ) ;
#14351=SURFACE_STYLE_USAGE ( .BOTH. , #460 ) ;
#14405=DIRECTION ( 'NONE',  ( 1.224646799147350002E-16, -1.000000000000000000, -6.123233995736759873E-17 ) ) ;
#14439=VECTOR ( 'NONE', #12030, 1000.000000000000000 ) ;
#14455=AXIS2_PLACEMENT_3D ( 'NONE', #3247, #4359, #8632 ) ;
#14496=ORIENTED_EDGE ( 'NONE', *, *, #11416, .T. ) ;
#14500=CARTESIAN_POINT ( 'NONE',  ( -2.350000000000000089, -5.599999999999999645, 6.400000000000000355 ) ) ;
#14503=VECTOR ( 'NONE', #1830, 1000.000000000000227 ) ;
#14561=EDGE_CURVE ( 'NONE', #14614, #2121, #9223, .T. ) ;
#14614=VERTEX_POINT ( 'NONE', #15258 ) ;
#14643=CARTESIAN_POINT ( 'NONE',  ( 1.550000000000000044, -5.599999999999999645, 5.100000000000000533 ) ) ;
#14675=EDGE_CURVE ( 'NONE', #4371, #2194, #7115, .T. ) ;
#14722=DIRECTION ( 'NONE',  ( 0.000000000000000000, -1.000000000000000000, 0.000000000000000000 ) ) ;
#14724=AXIS2_PLACEMENT_3D ( 'NONE', #16813, #15252, #15166 ) ;
#14877=PLANE ( 'NONE',  #926 ) ;
#14900=VERTEX_POINT ( 'NONE', #9972 ) ;
#14905=LINE ( 'NONE', #13231, #14439 ) ;
#14928=VERTEX_POINT ( 'NONE', #14314 ) ;
#14988=DIRECTION ( 'NONE',  ( 2.220446049250309876E-16, 0.000000000000000000, 1.000000000000000000 ) ) ;
#15000=DIRECTION ( 'NONE',  ( 2.865091676452019757E-16, 0.000000000000000000, -1.000000000000000000 ) ) ;
#15065=EDGE_CURVE ( 'NONE', #13803, #8938, #6414, .T. ) ;
#15111=DIRECTION ( 'NONE',  ( 0.3420201433256691015, 0.000000000000000000, -0.9396926207859082059 ) ) ;
#15139=FACE_OUTER_BOUND ( 'NONE', #4129, .T. ) ;
#15166=DIRECTION ( 'NONE',  ( 0.000000000000000000, 0.000000000000000000, -1.000000000000000000 ) ) ;
#15185=LINE ( 'NONE', #3779, #8872 ) ;
#15190=DIRECTION ( 'NONE',  ( 0.000000000000000000, -1.000000000000000000, 0.000000000000000000 ) ) ;
#15227=DIRECTION ( 'NONE',  ( 0.000000000000000000, 0.000000000000000000, 1.000000000000000000 ) ) ;
#15252=DIRECTION ( 'NONE',  ( 1.224646799147350002E-16, -1.000000000000000000, -6.123233995736759873E-17 ) ) ;
#15258=CARTESIAN_POINT ( 'NONE',  ( -1.000000000000000000, -6.000000000000000000, 3.673738709727309981 ) ) ;
#15351=AXIS2_PLACEMENT_3D ( 'NONE', #2145, #13439, #10294 ) ;
#15358=VECTOR ( 'NONE', #10182, 1000.000000000000000 ) ;
#15430=VERTEX_POINT ( 'NONE', #8565 ) ;
#15454=ORIENTED_EDGE ( 'NONE', *, *, #11572, .T. ) ;
#15480=ORIENTED_EDGE ( 'NONE', *, *, #6879, .F. ) ;
#15511=( NAMED_UNIT ( * ) PLANE_ANGLE_UNIT ( ) SI_UNIT ( $, .RADIAN. ) );
#15525=LINE ( 'NONE', #8388, #9549 ) ;
#15533=PLANE ( 'NONE',  #8317 ) ;
#15545=DIRECTION ( 'NONE',  ( 0.000000000000000000, 0.000000000000000000, 1.000000000000000000 ) ) ;
#15604=VECTOR ( 'NONE', #1046, 1000.000000000000000 ) ;
#15639=( GEOMETRIC_REPRESENTATION_CONTEXT ( 3 ) GLOBAL_UNCERTAINTY_ASSIGNED_CONTEXT ( ( #6949 ) ) GLOBAL_UNIT_ASSIGNED_CONTEXT ( ( #294, #10273, #1935 ) ) REPRESENTATION_CONTEXT ( 'NONE', 'WORKASPACE' ) );
#15670=ORIENTED_EDGE ( 'NONE', *, *, #15065, .F. ) ;
#15678=DIRECTION ( 'NONE',  ( 0.000000000000000000, -1.000000000000000000, 0.000000000000000000 ) ) ;
#15696=VECTOR ( 'NONE', #15807, 1000.000000000000000 ) ;
#15702=DIRECTION ( 'NONE',  ( -1.000000000000000000, 0.000000000000000000, 0.000000000000000000 ) ) ;
#15706=CARTESIAN_POINT ( 'NONE',  ( 1.500000000000000000, -5.599999999999999645, 2.299999999999999822 ) ) ;
#15707=VERTEX_POINT ( 'NONE', #6853 ) ;
#15737=ORIENTED_EDGE ( 'NONE', *, *, #13264, .F. ) ;
#15769=EDGE_CURVE ( 'NONE', #16005, #13449, #12499, .T. ) ;
#15803=VECTOR ( 'NONE', #2513, 1000.000000000000000 ) ;
#15807=DIRECTION ( 'NONE',  ( 0.000000000000000000, 0.000000000000000000, 1.000000000000000000 ) ) ;
#15862=CARTESIAN_POINT ( 'NONE',  ( 2.350000000000000089, -5.599999999999999645, 2.799999999999999822 ) ) ;
#15868=ORIENTED_EDGE ( 'NONE', *, *, #12439, .T. ) ;
#15958=VERTEX_POINT ( 'NONE', #5066 ) ;
#15992=ORIENTED_EDGE ( 'NONE', *, *, #11553, .T. ) ;
#15997=ORIENTED_EDGE ( 'NONE', *, *, #2918, .T. ) ;
#16004=SHAPE_REPRESENTATION ( 'Actuator Spring Stop Clip', ( #17681 ), #5599 ) ;
#16005=VERTEX_POINT ( 'NONE', #2403 ) ;
#16050=EDGE_CURVE ( 'NONE', #9915, #2194, #8050, .T. ) ;
#16051=AXIS2_PLACEMENT_3D ( 'NONE', #7925, #3645, #3128 ) ;
#16070=EDGE_CURVE ( 'NONE', #7170, #10479, #2301, .T. ) ;
#16087=ADVANCED_FACE ( 'NONE', ( #715 ), #10627, .T. ) ;
#16137=ORIENTED_EDGE ( 'NONE', *, *, #9271, .T. ) ;
#16173=VECTOR ( 'NONE', #1205, 1000.000000000000000 ) ;
#16261=ORIENTED_EDGE ( 'NONE', *, *, #7213, .T. ) ;
#16313=LINE ( 'NONE', #11876, #9499 ) ;
#16332=VECTOR ( 'NONE', #12739, 1000.000000000000000 ) ;
#16355=CARTESIAN_POINT ( 'NONE',  ( 1.850000000000000089, -6.000000000000000000, 2.299999999999999822 ) ) ;
#16381=ADVANCED_FACE ( 'NONE', ( #7543 ), #425, .T. ) ;
#16388=DIRECTION ( 'NONE',  ( 1.224646799147350002E-16, -1.000000000000000000, -6.123233995736769734E-17 ) ) ;
#16389=ADVANCED_FACE ( 'NONE', ( #3024 ), #11815, .T. ) ;
#16422=ORIENTED_EDGE ( 'NONE', *, *, #4561, .T. ) ;
#16430=LINE ( 'NONE', #10882, #3217 ) ;
#16446=ORIENTED_EDGE ( 'NONE', *, *, #4561, .F. ) ;
#16459=DIRECTION ( 'NONE',  ( 1.224646799147350002E-16, -1.000000000000000000, -6.123233995736769734E-17 ) ) ;
#16475=LINE ( 'NONE', #9538, #3167 ) ;
#16593=PRODUCT_DEFINITION_CONTEXT ( 'detailed design', #7798, 'design' ) ;
#16624=DIRECTION ( 'NONE',  ( 1.000000000000000000, 0.000000000000000000, 2.865091676452019757E-16 ) ) ;
#16656=CARTESIAN_POINT ( 'NONE',  ( -2.350000000000000089, -6.000000000000000000, 2.799999999999999822 ) ) ;
#16694=DIRECTION ( 'NONE',  ( 1.000000000000000000, 0.000000000000000000, 0.000000000000000000 ) ) ;
#16712=ORIENTED_EDGE ( 'NONE', *, *, #5201, .T. ) ;
#16730=LINE ( 'NONE', #16830, #8956 ) ;
#16744=AXIS2_PLACEMENT_3D ( 'NONE', #2505, #13330, #9450 ) ;
#16759=VERTEX_POINT ( 'NONE', #11252 ) ;
#16775=STYLED_ITEM ( 'NONE', ( #380 ), #7785 ) ;
#16813=CARTESIAN_POINT ( 'NONE',  ( 1.850000000000000089, -5.599999999999999645, 2.799999999999999822 ) ) ;
#16830=CARTESIAN_POINT ( 'NONE',  ( -1.550000000000000044, -5.599999999999999645, 5.100000000000000533 ) ) ;
#16834=EDGE_LOOP ( 'NONE', ( #16261, #14184, #5297, #8451 ) ) ;
#16836=DIRECTION ( 'NONE',  ( 0.000000000000000000, 0.000000000000000000, 1.000000000000000000 ) ) ;
#16838=ORIENTED_EDGE ( 'NONE', *, *, #2719, .F. ) ;
#16858=ORIENTED_EDGE ( 'NONE', *, *, #5093, .F. ) ;
#16920=LINE ( 'NONE', #7554, #17432 ) ;
#16927=EDGE_CURVE ( 'NONE', #2194, #917, #9986, .T. ) ;
#16954=DIRECTION ( 'NONE',  ( 1.000000000000000000, 0.000000000000000000, 0.000000000000000000 ) ) ;
#16972=CARTESIAN_POINT ( 'NONE',  ( 1.000000000000000000, -5.599999999999999645, 5.100000000000000533 ) ) ;
#17012=LINE ( 'NONE', #12775, #10256 ) ;
#17049=AXIS2_PLACEMENT_3D ( 'NONE', #6349, #3768, #12013 ) ;
#17223=PLANE ( 'NONE',  #9739 ) ;
#17289=CARTESIAN_POINT ( 'NONE',  ( 2.350000000000000089, -6.000000000000000000, 2.799999999999999822 ) ) ;
#17327=CLOSED_SHELL ( 'NONE', ( #4564, #8351, #16381, #1983, #12315, #3256, #9631, #17594, #12479, #13324, #9007, #5388, #10063, #3941, #16087, #17884, #5855, #13924, #934, #16389 ) ) ;
#17377=AXIS2_PLACEMENT_3D ( 'NONE', #29, #12883, #16954 ) ;
#17432=VECTOR ( 'NONE', #10337, 1000.000000000000000 ) ;
#17449=DIRECTION ( 'NONE',  ( -1.000000000000000000, 0.000000000000000000, 0.000000000000000000 ) ) ;
#17452=ORIENTED_EDGE ( 'NONE', *, *, #4599, .F. ) ;
#17478=CARTESIAN_POINT ( 'NONE',  ( -2.350000000000000089, -6.000000000000000000, 6.400000000000000355 ) ) ;
#17532=VERTEX_POINT ( 'NONE', #12284 ) ;
#17547=LINE ( 'NONE', #10917, #13553 ) ;
#17558=CARTESIAN_POINT ( 'NONE',  ( 1.000000000000000000, -5.599999999999999645, 3.673738709727309981 ) ) ;
#17594=ADVANCED_FACE ( 'NONE', ( #18275 ), #12380, .T. ) ;
#17598=CARTESIAN_POINT ( 'NONE',  ( 1.500000000000000000, -5.599999999999999645, 2.299999999999999822 ) ) ;
#17615=CARTESIAN_POINT ( 'NONE',  ( -1.550000000000000044, -5.599999999999999645, 6.100000000000000533 ) ) ;
#17622=ORIENTED_EDGE ( 'NONE', *, *, #9762, .F. ) ;
#17641=CARTESIAN_POINT ( 'NONE',  ( 1.850000000000000089, -6.000000000000000000, 6.899999999999999467 ) ) ;
#17651=VECTOR ( 'NONE', #3091, 1000.000000000000000 ) ;
#17665=DIRECTION ( 'NONE',  ( -1.556829778943089964E-16, 0.000000000000000000, 1.000000000000000000 ) ) ;
#17669=CARTESIAN_POINT ( 'NONE',  ( 1.550000000000000044, -6.000000000000000000, 6.100000000000000533 ) ) ;
#17681=AXIS2_PLACEMENT_3D ( 'NONE', #11191, #16836, #4146 ) ;
#17738=CARTESIAN_POINT ( 'NONE',  ( -2.350000000000000089, -5.599999999999999645, 2.799999999999999822 ) ) ;
#17758=FACE_OUTER_BOUND ( 'NONE', #7188, .T. ) ;
#17769=ORIENTED_EDGE ( 'NONE', *, *, #2305, .F. ) ;
#17778=CARTESIAN_POINT ( 'NONE',  ( 1.550000000000000044, -5.599999999999999645, 6.100000000000000533 ) ) ;
#17831=DIRECTION ( 'NONE',  ( 0.000000000000000000, -1.000000000000000000, 0.000000000000000000 ) ) ;
#17834=FACE_OUTER_BOUND ( 'NONE', #2420, .T. ) ;
#17884=ADVANCED_FACE ( 'NONE', ( #15139 ), #8375, .T. ) ;
#17973=CIRCLE ( 'NONE', #12677, 0.4999999999999995559 ) ;
#17985=DIRECTION ( 'NONE',  ( 0.000000000000000000, -1.000000000000000000, 0.000000000000000000 ) ) ;
#18004=ORIENTED_EDGE ( 'NONE', *, *, #14561, .T. ) ;
#18129=DIRECTION ( 'NONE',  ( 0.9396926207859082059, 0.000000000000000000, -0.3420201433256691015 ) ) ;
#18146=EDGE_CURVE ( 'NONE', #15707, #2630, #18273, .T. ) ;
#18175=DIRECTION ( 'NONE',  ( 0.000000000000000000, 0.000000000000000000, -1.000000000000000000 ) ) ;
#18230=DIRECTION ( 'NONE',  ( 1.000000000000000000, 0.000000000000000000, 0.000000000000000000 ) ) ;
#18273=CIRCLE ( 'NONE', #15351, 0.5000000000000000000 ) ;
#18275=FACE_OUTER_BOUND ( 'NONE', #3013, .T. ) ;
#18277=ORIENTED_EDGE ( 'NONE', *, *, #11553, .F. ) ;
ENDSEC;
END-ISO-10303-21;
